ISO-10303-21;
HEADER;
/* Generated by software containing ST-Developer
 * from STEP Tools, Inc. (www.steptools.com) 
 */

FILE_DESCRIPTION(
/* description */ ('Wall-mounted air drop station'),
/* implementation_level */ '2;1');

FILE_NAME(
/* name */ 'Bulkhead retaining nut.step',
/* time_stamp */ '2026-10-28T22:16:19-07:00',
/* author */ (''),
/* organization */ (''),
/* preprocessor_version */ 'ST-DEVELOPER v20.2',
/* originating_system */ 'Autodesk Translation Framework v15.17.0.0',
/* authorisation */ '');

FILE_SCHEMA (('AUTOMOTIVE_DESIGN { 1 0 10303 214 3 1 1 }'));
ENDSEC;

DATA;
#10=MECHANICAL_DESIGN_GEOMETRIC_PRESENTATION_REPRESENTATION('',(#347),#10517);
#289=SHAPE_REPRESENTATION_RELATIONSHIP('SRR','None',#10646,#318);
#318=ADVANCED_BREP_SHAPE_REPRESENTATION('',(#376),#10490);
#347=STYLED_ITEM('',(#10881),#376);
#376=MANIFOLD_SOLID_BREP('Body1',#5886);
#426=FACE_BOUND('',#1198,.T.);
#427=FACE_BOUND('',#1200,.T.);
#559=PLANE('',#6337);
#560=PLANE('',#6338);
#561=PLANE('',#6339);
#562=PLANE('',#6340);
#563=PLANE('',#6341);
#564=PLANE('',#6342);
#565=PLANE('',#6343);
#566=PLANE('',#6344);
#808=FACE_OUTER_BOUND('',#1190,.T.);
#809=FACE_OUTER_BOUND('',#1191,.T.);
#810=FACE_OUTER_BOUND('',#1192,.T.);
#811=FACE_OUTER_BOUND('',#1193,.T.);
#812=FACE_OUTER_BOUND('',#1194,.T.);
#813=FACE_OUTER_BOUND('',#1195,.T.);
#814=FACE_OUTER_BOUND('',#1196,.T.);
#815=FACE_OUTER_BOUND('',#1197,.T.);
#816=FACE_OUTER_BOUND('',#1199,.T.);
#1190=EDGE_LOOP('',(#4201,#4202,#4203,#4204));
#1191=EDGE_LOOP('',(#4205,#4206,#4207,#4208));
#1192=EDGE_LOOP('',(#4209,#4210,#4211,#4212));
#1193=EDGE_LOOP('',(#4213,#4214,#4215,#4216));
#1194=EDGE_LOOP('',(#4217,#4218,#4219,#4220));
#1195=EDGE_LOOP('',(#4221,#4222,#4223,#4224));
#1196=EDGE_LOOP('',(#4225,#4226,#4227,#4228));
#1197=EDGE_LOOP('',(#4229,#4230,#4231,#4232,#4233,#4234));
#1198=EDGE_LOOP('',(#4235));
#1199=EDGE_LOOP('',(#4236,#4237,#4238,#4239,#4240,#4241));
#1200=EDGE_LOOP('',(#4242));
#1666=LINE('',#9019,#2130);
#1667=LINE('',#9024,#2131);
#1668=LINE('',#9026,#2132);
#1669=LINE('',#9028,#2133);
#1670=LINE('',#9029,#2134);
#1671=LINE('',#9032,#2135);
#1672=LINE('',#9034,#2136);
#1673=LINE('',#9035,#2137);
#1674=LINE('',#9038,#2138);
#1675=LINE('',#9040,#2139);
#1676=LINE('',#9041,#2140);
#1677=LINE('',#9044,#2141);
#1678=LINE('',#9046,#2142);
#1679=LINE('',#9047,#2143);
#1680=LINE('',#9050,#2144);
#1681=LINE('',#9052,#2145);
#1682=LINE('',#9053,#2146);
#1683=LINE('',#9055,#2147);
#1684=LINE('',#9056,#2148);
#2130=VECTOR('',#7200,0.57);
#2131=VECTOR('',#7205,1.);
#2132=VECTOR('',#7206,1.);
#2133=VECTOR('',#7207,1.);
#2134=VECTOR('',#7208,1.);
#2135=VECTOR('',#7211,1.);
#2136=VECTOR('',#7212,1.);
#2137=VECTOR('',#7213,1.);
#2138=VECTOR('',#7216,1.);
#2139=VECTOR('',#7217,1.);
#2140=VECTOR('',#7218,1.);
#2141=VECTOR('',#7221,1.);
#2142=VECTOR('',#7222,1.);
#2143=VECTOR('',#7223,1.);
#2144=VECTOR('',#7226,1.);
#2145=VECTOR('',#7227,1.);
#2146=VECTOR('',#7228,1.);
#2147=VECTOR('',#7231,1.);
#2148=VECTOR('',#7232,1.);
#2560=CIRCLE('',#6335,0.57);
#2561=CIRCLE('',#6336,0.57);
#2841=VERTEX_POINT('',#9016);
#2842=VERTEX_POINT('',#9018);
#2843=VERTEX_POINT('',#9022);
#2844=VERTEX_POINT('',#9023);
#2845=VERTEX_POINT('',#9025);
#2846=VERTEX_POINT('',#9027);
#2847=VERTEX_POINT('',#9031);
#2848=VERTEX_POINT('',#9033);
#2849=VERTEX_POINT('',#9037);
#2850=VERTEX_POINT('',#9039);
#2851=VERTEX_POINT('',#9043);
#2852=VERTEX_POINT('',#9045);
#2853=VERTEX_POINT('',#9049);
#2854=VERTEX_POINT('',#9051);
#3358=EDGE_CURVE('',#2841,#2841,#2560,.T.);
#3359=EDGE_CURVE('',#2841,#2842,#1666,.T.);
#3360=EDGE_CURVE('',#2842,#2842,#2561,.T.);
#3361=EDGE_CURVE('',#2843,#2844,#1667,.T.);
#3362=EDGE_CURVE('',#2844,#2845,#1668,.T.);
#3363=EDGE_CURVE('',#2846,#2845,#1669,.T.);
#3364=EDGE_CURVE('',#2843,#2846,#1670,.T.);
#3365=EDGE_CURVE('',#2847,#2843,#1671,.T.);
#3366=EDGE_CURVE('',#2848,#2846,#1672,.T.);
#3367=EDGE_CURVE('',#2847,#2848,#1673,.T.);
#3368=EDGE_CURVE('',#2849,#2847,#1674,.T.);
#3369=EDGE_CURVE('',#2850,#2848,#1675,.T.);
#3370=EDGE_CURVE('',#2849,#2850,#1676,.T.);
#3371=EDGE_CURVE('',#2851,#2849,#1677,.T.);
#3372=EDGE_CURVE('',#2852,#2850,#1678,.T.);
#3373=EDGE_CURVE('',#2851,#2852,#1679,.T.);
#3374=EDGE_CURVE('',#2853,#2851,#1680,.T.);
#3375=EDGE_CURVE('',#2854,#2852,#1681,.T.);
#3376=EDGE_CURVE('',#2853,#2854,#1682,.T.);
#3377=EDGE_CURVE('',#2844,#2853,#1683,.T.);
#3378=EDGE_CURVE('',#2845,#2854,#1684,.T.);
#4201=ORIENTED_EDGE('',*,*,#3358,.F.);
#4202=ORIENTED_EDGE('',*,*,#3359,.T.);
#4203=ORIENTED_EDGE('',*,*,#3360,.F.);
#4204=ORIENTED_EDGE('',*,*,#3359,.F.);
#4205=ORIENTED_EDGE('',*,*,#3361,.T.);
#4206=ORIENTED_EDGE('',*,*,#3362,.T.);
#4207=ORIENTED_EDGE('',*,*,#3363,.F.);
#4208=ORIENTED_EDGE('',*,*,#3364,.F.);
#4209=ORIENTED_EDGE('',*,*,#3365,.T.);
#4210=ORIENTED_EDGE('',*,*,#3364,.T.);
#4211=ORIENTED_EDGE('',*,*,#3366,.F.);
#4212=ORIENTED_EDGE('',*,*,#3367,.F.);
#4213=ORIENTED_EDGE('',*,*,#3368,.T.);
#4214=ORIENTED_EDGE('',*,*,#3367,.T.);
#4215=ORIENTED_EDGE('',*,*,#3369,.F.);
#4216=ORIENTED_EDGE('',*,*,#3370,.F.);
#4217=ORIENTED_EDGE('',*,*,#3371,.T.);
#4218=ORIENTED_EDGE('',*,*,#3370,.T.);
#4219=ORIENTED_EDGE('',*,*,#3372,.F.);
#4220=ORIENTED_EDGE('',*,*,#3373,.F.);
#4221=ORIENTED_EDGE('',*,*,#3374,.T.);
#4222=ORIENTED_EDGE('',*,*,#3373,.T.);
#4223=ORIENTED_EDGE('',*,*,#3375,.F.);
#4224=ORIENTED_EDGE('',*,*,#3376,.F.);
#4225=ORIENTED_EDGE('',*,*,#3377,.T.);
#4226=ORIENTED_EDGE('',*,*,#3376,.T.);
#4227=ORIENTED_EDGE('',*,*,#3378,.F.);
#4228=ORIENTED_EDGE('',*,*,#3362,.F.);
#4229=ORIENTED_EDGE('',*,*,#3378,.T.);
#4230=ORIENTED_EDGE('',*,*,#3375,.T.);
#4231=ORIENTED_EDGE('',*,*,#3372,.T.);
#4232=ORIENTED_EDGE('',*,*,#3369,.T.);
#4233=ORIENTED_EDGE('',*,*,#3366,.T.);
#4234=ORIENTED_EDGE('',*,*,#3363,.T.);
#4235=ORIENTED_EDGE('',*,*,#3360,.T.);
#4236=ORIENTED_EDGE('',*,*,#3377,.F.);
#4237=ORIENTED_EDGE('',*,*,#3361,.F.);
#4238=ORIENTED_EDGE('',*,*,#3365,.F.);
#4239=ORIENTED_EDGE('',*,*,#3368,.F.);
#4240=ORIENTED_EDGE('',*,*,#3371,.F.);
#4241=ORIENTED_EDGE('',*,*,#3374,.F.);
#4242=ORIENTED_EDGE('',*,*,#3358,.T.);
#5451=CYLINDRICAL_SURFACE('',#6334,0.57);
#5581=ADVANCED_FACE('',(#808),#5451,.F.);
#5582=ADVANCED_FACE('',(#809),#559,.T.);
#5583=ADVANCED_FACE('',(#810),#560,.T.);
#5584=ADVANCED_FACE('',(#811),#561,.T.);
#5585=ADVANCED_FACE('',(#812),#562,.T.);
#5586=ADVANCED_FACE('',(#813),#563,.T.);
#5587=ADVANCED_FACE('',(#814),#564,.T.);
#5588=ADVANCED_FACE('',(#815,#426),#565,.T.);
#5589=ADVANCED_FACE('',(#816,#427),#566,.F.);
#5886=CLOSED_SHELL('',(#5581,#5582,#5583,#5584,#5585,#5586,#5587,#5588,
#5589));
#6333=AXIS2_PLACEMENT_3D('',#9014,#7194,#7195);
#6334=AXIS2_PLACEMENT_3D('',#9015,#7196,#7197);
#6335=AXIS2_PLACEMENT_3D('',#9017,#7198,#7199);
#6336=AXIS2_PLACEMENT_3D('',#9020,#7201,#7202);
#6337=AXIS2_PLACEMENT_3D('',#9021,#7203,#7204);
#6338=AXIS2_PLACEMENT_3D('',#9030,#7209,#7210);
#6339=AXIS2_PLACEMENT_3D('',#9036,#7214,#7215);
#6340=AXIS2_PLACEMENT_3D('',#9042,#7219,#7220);
#6341=AXIS2_PLACEMENT_3D('',#9048,#7224,#7225);
#6342=AXIS2_PLACEMENT_3D('',#9054,#7229,#7230);
#6343=AXIS2_PLACEMENT_3D('',#9057,#7233,#7234);
#6344=AXIS2_PLACEMENT_3D('',#9058,#7235,#7236);
#7194=DIRECTION('axis',(0.,0.,1.));
#7195=DIRECTION('refdir',(1.,0.,0.));
#7196=DIRECTION('center_axis',(1.,0.,0.));
#7197=DIRECTION('ref_axis',(0.,0.,-1.));
#7198=DIRECTION('center_axis',(1.,0.,0.));
#7199=DIRECTION('ref_axis',(0.,0.,-1.));
#7200=DIRECTION('',(1.,0.,0.));
#7201=DIRECTION('center_axis',(-1.,0.,0.));
#7202=DIRECTION('ref_axis',(0.,0.,-1.));
#7203=DIRECTION('center_axis',(0.,0.,-1.));
#7204=DIRECTION('ref_axis',(0.,1.,0.));
#7205=DIRECTION('',(0.,1.,0.));
#7206=DIRECTION('',(1.,0.,0.));
#7207=DIRECTION('',(0.,1.,0.));
#7208=DIRECTION('',(1.,0.,0.));
#7209=DIRECTION('center_axis',(0.,-0.866025403784439,-0.499999999999999));
#7210=DIRECTION('ref_axis',(0.,0.499999999999999,-0.866025403784439));
#7211=DIRECTION('',(0.,0.499999999999999,-0.866025403784439));
#7212=DIRECTION('',(0.,0.499999999999999,-0.866025403784439));
#7213=DIRECTION('',(1.,0.,0.));
#7214=DIRECTION('center_axis',(0.,-0.866025403784439,0.499999999999999));
#7215=DIRECTION('ref_axis',(0.,-0.499999999999999,-0.866025403784439));
#7216=DIRECTION('',(0.,-0.499999999999999,-0.866025403784439));
#7217=DIRECTION('',(0.,-0.499999999999999,-0.866025403784439));
#7218=DIRECTION('',(1.,0.,0.));
#7219=DIRECTION('center_axis',(0.,0.,1.));
#7220=DIRECTION('ref_axis',(0.,-1.,0.));
#7221=DIRECTION('',(0.,-1.,0.));
#7222=DIRECTION('',(0.,-1.,0.));
#7223=DIRECTION('',(1.,0.,0.));
#7224=DIRECTION('center_axis',(0.,0.866025403784439,0.499999999999999));
#7225=DIRECTION('ref_axis',(0.,-0.499999999999999,0.866025403784439));
#7226=DIRECTION('',(0.,-0.499999999999999,0.866025403784439));
#7227=DIRECTION('',(0.,-0.499999999999999,0.866025403784439));
#7228=DIRECTION('',(1.,0.,0.));
#7229=DIRECTION('center_axis',(0.,0.866025403784439,-0.499999999999999));
#7230=DIRECTION('ref_axis',(0.,0.499999999999999,0.866025403784439));
#7231=DIRECTION('',(0.,0.499999999999999,0.866025403784439));
#7232=DIRECTION('',(0.,0.499999999999999,0.866025403784439));
#7233=DIRECTION('center_axis',(1.,0.,0.));
#7234=DIRECTION('ref_axis',(0.,0.,-1.));
#7235=DIRECTION('center_axis',(1.,0.,0.));
#7236=DIRECTION('ref_axis',(0.,0.,-1.));
#9014=CARTESIAN_POINT('',(0.,0.,0.));
#9015=CARTESIAN_POINT('Origin',(-5.1,-12.4,5.));
#9016=CARTESIAN_POINT('',(-5.,-12.4,5.57));
#9017=CARTESIAN_POINT('Origin',(-5.,-12.4,5.));
#9018=CARTESIAN_POINT('',(-4.4,-12.4,5.57));
#9019=CARTESIAN_POINT('',(-5.1,-12.4,5.57));
#9020=CARTESIAN_POINT('Origin',(-4.4,-12.4,5.));
#9021=CARTESIAN_POINT('Origin',(-5.,-12.9484827557301,4.05));
#9022=CARTESIAN_POINT('',(-5.,-12.9484827557301,4.05));
#9023=CARTESIAN_POINT('',(-5.,-11.8515172442699,4.05));
#9024=CARTESIAN_POINT('',(-5.,-12.9484827557301,4.05));
#9025=CARTESIAN_POINT('',(-4.4,-11.8515172442699,4.05));
#9026=CARTESIAN_POINT('',(-5.,-11.8515172442699,4.05));
#9027=CARTESIAN_POINT('',(-4.4,-12.9484827557301,4.05));
#9028=CARTESIAN_POINT('',(-4.4,-12.9484827557301,4.05));
#9029=CARTESIAN_POINT('',(-5.,-12.9484827557301,4.05));
#9030=CARTESIAN_POINT('Origin',(-5.,-13.4969655114603,5.));
#9031=CARTESIAN_POINT('',(-5.,-13.4969655114603,5.));
#9032=CARTESIAN_POINT('',(-5.,-13.4969655114603,5.));
#9033=CARTESIAN_POINT('',(-4.4,-13.4969655114603,5.));
#9034=CARTESIAN_POINT('',(-4.4,-13.4969655114603,5.));
#9035=CARTESIAN_POINT('',(-5.,-13.4969655114603,5.));
#9036=CARTESIAN_POINT('Origin',(-5.,-12.9484827557301,5.95));
#9037=CARTESIAN_POINT('',(-5.,-12.9484827557301,5.95));
#9038=CARTESIAN_POINT('',(-5.,-12.9484827557301,5.95));
#9039=CARTESIAN_POINT('',(-4.4,-12.9484827557301,5.95));
#9040=CARTESIAN_POINT('',(-4.4,-12.9484827557301,5.95));
#9041=CARTESIAN_POINT('',(-5.,-12.9484827557301,5.95));
#9042=CARTESIAN_POINT('Origin',(-5.,-11.8515172442699,5.95));
#9043=CARTESIAN_POINT('',(-5.,-11.8515172442699,5.95));
#9044=CARTESIAN_POINT('',(-5.,-11.8515172442699,5.95));
#9045=CARTESIAN_POINT('',(-4.4,-11.8515172442699,5.95));
#9046=CARTESIAN_POINT('',(-4.4,-11.8515172442699,5.95));
#9047=CARTESIAN_POINT('',(-5.,-11.8515172442699,5.95));
#9048=CARTESIAN_POINT('Origin',(-5.,-11.3030344885397,5.));
#9049=CARTESIAN_POINT('',(-5.,-11.3030344885397,5.));
#9050=CARTESIAN_POINT('',(-5.,-11.3030344885397,5.));
#9051=CARTESIAN_POINT('',(-4.4,-11.3030344885397,5.));
#9052=CARTESIAN_POINT('',(-4.4,-11.3030344885397,5.));
#9053=CARTESIAN_POINT('',(-5.,-11.3030344885397,5.));
#9054=CARTESIAN_POINT('Origin',(-5.,-11.8515172442699,4.05));
#9055=CARTESIAN_POINT('',(-5.,-11.8515172442699,4.05));
#9056=CARTESIAN_POINT('',(-4.4,-11.8515172442699,4.05));
#9057=CARTESIAN_POINT('Origin',(-4.4,-12.4,5.));
#9058=CARTESIAN_POINT('Origin',(-5.,-12.4,5.));
#10457=UNCERTAINTY_MEASURE_WITH_UNIT(LENGTH_MEASURE(0.001),#10518,
'DISTANCE_ACCURACY_VALUE',
'Maximum model space distance between geometric entities at asserted c
onnectivities');
#10484=UNCERTAINTY_MEASURE_WITH_UNIT(LENGTH_MEASURE(0.001),#10518,
'DISTANCE_ACCURACY_VALUE',
'Maximum model space distance between geometric entities at asserted c
onnectivities');
#10490=(
GEOMETRIC_REPRESENTATION_CONTEXT(3)
GLOBAL_UNCERTAINTY_ASSIGNED_CONTEXT((#10457))
GLOBAL_UNIT_ASSIGNED_CONTEXT((#10518,#10520,#10521))
REPRESENTATION_CONTEXT('','3D')
);
#10517=(
GEOMETRIC_REPRESENTATION_CONTEXT(3)
GLOBAL_UNCERTAINTY_ASSIGNED_CONTEXT((#10484))
GLOBAL_UNIT_ASSIGNED_CONTEXT((#10518,#10520,#10521))
REPRESENTATION_CONTEXT('','3D')
);
#10518=(
LENGTH_UNIT()
NAMED_UNIT(*)
SI_UNIT(.CENTI.,.METRE.)
);
#10520=(
NAMED_UNIT(*)
PLANE_ANGLE_UNIT()
SI_UNIT($,.RADIAN.)
);
#10521=(
NAMED_UNIT(*)
SI_UNIT($,.STERADIAN.)
SOLID_ANGLE_UNIT()
);
#10527=SHAPE_DEFINITION_REPRESENTATION(#10559,#10646);
#10559=PRODUCT_DEFINITION_SHAPE('',$,#10679);
#10646=SHAPE_REPRESENTATION('',(#6333),#10490);
#10673=PRODUCT_DEFINITION_CONTEXT('part definition',#10771,'design');
#10679=PRODUCT_DEFINITION('Bulkhead retaining nut',
'Bulkhead retaining nut',#10711,#10673);
#10711=PRODUCT_DEFINITION_FORMATION('',$,#10778);
#10771=APPLICATION_CONTEXT(
'Core Data for Automotive Mechanical Design Process');
#10772=PRODUCT_CONTEXT('part definition',#10771,'mechanical');
#10778=PRODUCT('Bulkhead retaining nut','Bulkhead retaining nut',
'Bulkhead retaining nut',(#10772));
#10875=COLOUR_RGB('Black',0.12,0.14,0.17);
#10876=FILL_AREA_STYLE_COLOUR('',#10875);
#10877=FILL_AREA_STYLE('',(#10876));
#10878=SURFACE_STYLE_FILL_AREA(#10877);
#10879=SURFACE_SIDE_STYLE('',(#10878));
#10880=SURFACE_STYLE_USAGE(.BOTH.,#10879);
#10881=PRESENTATION_STYLE_ASSIGNMENT((#10880));
ENDSEC;
END-ISO-10303-21;
